ISO-10303-21;
HEADER;
/* Generated by software containing ST-Developer
 * from STEP Tools, Inc. (www.steptools.com) 
 */

FILE_DESCRIPTION(
/* description */ ('STEP AP214'),
/* implementation_level */ '2;1');

FILE_NAME(
/* name */ 'Button Head Cap Screw M4x0.7x8.step',
/* time_stamp */ '2026-11-14T22:03:06-08:00',
/* author */ (''),
/* organization */ (''),
/* preprocessor_version */ 'ST-DEVELOPER v20.2',
/* originating_system */ 'Autodesk Translation Framework v15.17.0.0',
/* authorisation */ '');

FILE_SCHEMA (('AUTOMOTIVE_DESIGN { 1 0 10303 214 3 1 1 }'));
ENDSEC;

DATA;
#10=MECHANICAL_DESIGN_GEOMETRIC_PRESENTATION_REPRESENTATION('',(#312),#12966);
#152=SPHERICAL_SURFACE('',#6098,4.3249693283142);
#156=TOROIDAL_SURFACE('',#6087,2.2,0.2);
#161=CONICAL_SURFACE('',#6080,1732.05080756886,1.04719755119659);
#162=CONICAL_SURFACE('',#6091,1.61,0.785398163397447);
#292=SHAPE_REPRESENTATION_RELATIONSHIP('SRR','None',#13030,#300);
#300=ADVANCED_BREP_SHAPE_REPRESENTATION('',(#324),#12963);
#312=STYLED_ITEM('',(#13075),#324);
#324=MANIFOLD_SOLID_BREP('Body1',#5587);
#380=FACE_BOUND('',#1168,.T.);
#381=FACE_BOUND('',#1170,.T.);
#382=FACE_BOUND('',#1172,.T.);
#505=PLANE('',#6100);
#506=PLANE('',#6101);
#507=PLANE('',#6102);
#508=PLANE('',#6103);
#509=PLANE('',#6104);
#510=PLANE('',#6105);
#511=PLANE('',#6106);
#512=PLANE('',#6107);
#513=PLANE('',#6108);
#514=PLANE('',#6109);
#515=PLANE('',#6110);
#516=PLANE('',#6111);
#517=PLANE('',#6112);
#518=PLANE('',#6113);
#519=PLANE('',#6114);
#798=FACE_OUTER_BOUND('',#1162,.T.);
#799=FACE_OUTER_BOUND('',#1163,.T.);
#800=FACE_OUTER_BOUND('',#1164,.T.);
#801=FACE_OUTER_BOUND('',#1165,.T.);
#802=FACE_OUTER_BOUND('',#1166,.T.);
#803=FACE_OUTER_BOUND('',#1167,.T.);
#804=FACE_OUTER_BOUND('',#1169,.T.);
#805=FACE_OUTER_BOUND('',#1171,.T.);
#806=FACE_OUTER_BOUND('',#1173,.T.);
#807=FACE_OUTER_BOUND('',#1174,.T.);
#808=FACE_OUTER_BOUND('',#1175,.T.);
#809=FACE_OUTER_BOUND('',#1176,.T.);
#810=FACE_OUTER_BOUND('',#1177,.T.);
#811=FACE_OUTER_BOUND('',#1178,.T.);
#812=FACE_OUTER_BOUND('',#1179,.T.);
#813=FACE_OUTER_BOUND('',#1180,.T.);
#814=FACE_OUTER_BOUND('',#1181,.T.);
#815=FACE_OUTER_BOUND('',#1182,.T.);
#816=FACE_OUTER_BOUND('',#1183,.T.);
#817=FACE_OUTER_BOUND('',#1184,.T.);
#818=FACE_OUTER_BOUND('',#1185,.T.);
#1162=EDGE_LOOP('',(#4921,#4922,#4923,#4924,#4925,#4926,#4927,#4928));
#1163=EDGE_LOOP('',(#4929,#4930,#4931,#4932));
#1164=EDGE_LOOP('',(#4933,#4934,#4935,#4936));
#1165=EDGE_LOOP('',(#4937,#4938,#4939,#4940));
#1166=EDGE_LOOP('',(#4941,#4942,#4943,#4944));
#1167=EDGE_LOOP('',(#4945));
#1168=EDGE_LOOP('',(#4946));
#1169=EDGE_LOOP('',(#4947));
#1170=EDGE_LOOP('',(#4948,#4949,#4950,#4951,#4952,#4953));
#1171=EDGE_LOOP('',(#4954));
#1172=EDGE_LOOP('',(#4955));
#1173=EDGE_LOOP('',(#4956));
#1174=EDGE_LOOP('',(#4957,#4958,#4959,#4960,#4961));
#1175=EDGE_LOOP('',(#4962,#4963,#4964,#4965,#4966));
#1176=EDGE_LOOP('',(#4967,#4968,#4969,#4970,#4971));
#1177=EDGE_LOOP('',(#4972,#4973,#4974,#4975,#4976));
#1178=EDGE_LOOP('',(#4977,#4978,#4979,#4980,#4981));
#1179=EDGE_LOOP('',(#4982,#4983,#4984,#4985,#4986));
#1180=EDGE_LOOP('',(#4987,#4988,#4989));
#1181=EDGE_LOOP('',(#4990,#4991,#4992));
#1182=EDGE_LOOP('',(#4993,#4994,#4995));
#1183=EDGE_LOOP('',(#4996,#4997,#4998));
#1184=EDGE_LOOP('',(#4999,#5000,#5001));
#1185=EDGE_LOOP('',(#5002,#5003,#5004));
#1607=LINE('',#12646,#2064);
#1608=LINE('',#12668,#2065);
#1609=LINE('',#12671,#2066);
#1610=LINE('',#12676,#2067);
#1611=LINE('',#12684,#2068);
#1612=LINE('',#12686,#2069);
#1613=LINE('',#12688,#2070);
#1614=LINE('',#12690,#2071);
#1615=LINE('',#12692,#2072);
#1616=LINE('',#12693,#2073);
#1617=LINE('',#12698,#2074);
#1618=LINE('',#12700,#2075);
#1619=LINE('',#12701,#2076);
#1620=LINE('',#12702,#2077);
#1621=LINE('',#12704,#2078);
#1622=LINE('',#12706,#2079);
#1623=LINE('',#12707,#2080);
#1624=LINE('',#12709,#2081);
#1625=LINE('',#12711,#2082);
#1626=LINE('',#12712,#2083);
#1627=LINE('',#12714,#2084);
#1628=LINE('',#12716,#2085);
#1629=LINE('',#12717,#2086);
#1630=LINE('',#12719,#2087);
#1631=LINE('',#12721,#2088);
#1632=LINE('',#12722,#2089);
#1633=LINE('',#12724,#2090);
#1634=LINE('',#12725,#2091);
#2064=VECTOR('',#7399,1732.05080756886);
#2065=VECTOR('',#7424,1.61);
#2066=VECTOR('',#7429,2.);
#2067=VECTOR('',#7434,3.8);
#2068=VECTOR('',#7443,1000.);
#2069=VECTOR('',#7444,1000.);
#2070=VECTOR('',#7445,1000.);
#2071=VECTOR('',#7446,1000.);
#2072=VECTOR('',#7447,1000.);
#2073=VECTOR('',#7448,1000.);
#2074=VECTOR('',#7455,1000.);
#2075=VECTOR('',#7456,1000.);
#2076=VECTOR('',#7457,1000.);
#2077=VECTOR('',#7458,1000.);
#2078=VECTOR('',#7461,1000.);
#2079=VECTOR('',#7462,1000.);
#2080=VECTOR('',#7463,1000.);
#2081=VECTOR('',#7466,1000.);
#2082=VECTOR('',#7467,1000.);
#2083=VECTOR('',#7468,1000.);
#2084=VECTOR('',#7471,1000.);
#2085=VECTOR('',#7472,1000.);
#2086=VECTOR('',#7473,1000.);
#2087=VECTOR('',#7476,1000.);
#2088=VECTOR('',#7477,1000.);
#2089=VECTOR('',#7478,1000.);
#2090=VECTOR('',#7481,1000.);
#2091=VECTOR('',#7482,1000.);
#2334=CIRCLE('',#6081,1.25);
#2335=CIRCLE('',#6082,1.25);
#2336=CIRCLE('',#6083,1.25);
#2337=CIRCLE('',#6084,1.25);
#2338=CIRCLE('',#6085,1.25);
#2339=CIRCLE('',#6086,1.25);
#2340=CIRCLE('',#6088,2.2);
#2341=CIRCLE('',#6089,0.2);
#2342=CIRCLE('',#6090,2.);
#2343=CIRCLE('',#6092,2.);
#2344=CIRCLE('',#6093,1.61);
#2345=CIRCLE('',#6096,3.8);
#2346=CIRCLE('',#6097,3.8);
#2347=CIRCLE('',#6099,1.9);
#2800=VERTEX_POINT('',#12644);
#2801=VERTEX_POINT('',#12645);
#2802=VERTEX_POINT('',#12647);
#2803=VERTEX_POINT('',#12649);
#2804=VERTEX_POINT('',#12651);
#2805=VERTEX_POINT('',#12653);
#2806=VERTEX_POINT('',#12655);
#2807=VERTEX_POINT('',#12659);
#2808=VERTEX_POINT('',#12661);
#2809=VERTEX_POINT('',#12665);
#2810=VERTEX_POINT('',#12667);
#2811=VERTEX_POINT('',#12673);
#2812=VERTEX_POINT('',#12675);
#2813=VERTEX_POINT('',#12679);
#2814=VERTEX_POINT('',#12682);
#2815=VERTEX_POINT('',#12683);
#2816=VERTEX_POINT('',#12685);
#2817=VERTEX_POINT('',#12687);
#2818=VERTEX_POINT('',#12689);
#2819=VERTEX_POINT('',#12691);
#2820=VERTEX_POINT('',#12697);
#2821=VERTEX_POINT('',#12699);
#2822=VERTEX_POINT('',#12705);
#2823=VERTEX_POINT('',#12710);
#2824=VERTEX_POINT('',#12715);
#2825=VERTEX_POINT('',#12720);
#3517=EDGE_CURVE('',#2800,#2801,#1607,.T.);
#3518=EDGE_CURVE('',#2801,#2802,#2334,.T.);
#3519=EDGE_CURVE('',#2802,#2803,#2335,.T.);
#3520=EDGE_CURVE('',#2803,#2804,#2336,.T.);
#3521=EDGE_CURVE('',#2804,#2805,#2337,.T.);
#3522=EDGE_CURVE('',#2805,#2806,#2338,.T.);
#3523=EDGE_CURVE('',#2806,#2801,#2339,.T.);
#3524=EDGE_CURVE('',#2807,#2807,#2340,.T.);
#3525=EDGE_CURVE('',#2807,#2808,#2341,.T.);
#3526=EDGE_CURVE('',#2808,#2808,#2342,.T.);
#3527=EDGE_CURVE('',#2809,#2809,#2343,.T.);
#3528=EDGE_CURVE('',#2809,#2810,#1608,.T.);
#3529=EDGE_CURVE('',#2810,#2810,#2344,.T.);
#3530=EDGE_CURVE('',#2808,#2809,#1609,.T.);
#3531=EDGE_CURVE('',#2811,#2811,#2345,.T.);
#3532=EDGE_CURVE('',#2811,#2812,#1610,.T.);
#3533=EDGE_CURVE('',#2812,#2812,#2346,.T.);
#3534=EDGE_CURVE('',#2813,#2813,#2347,.T.);
#3535=EDGE_CURVE('',#2814,#2815,#1611,.T.);
#3536=EDGE_CURVE('',#2815,#2816,#1612,.T.);
#3537=EDGE_CURVE('',#2816,#2817,#1613,.T.);
#3538=EDGE_CURVE('',#2817,#2818,#1614,.T.);
#3539=EDGE_CURVE('',#2818,#2819,#1615,.T.);
#3540=EDGE_CURVE('',#2819,#2814,#1616,.T.);
#3541=EDGE_CURVE('',#2820,#2803,#1617,.T.);
#3542=EDGE_CURVE('',#2803,#2821,#1618,.T.);
#3543=EDGE_CURVE('',#2821,#2816,#1619,.T.);
#3544=EDGE_CURVE('',#2820,#2815,#1620,.T.);
#3545=EDGE_CURVE('',#2821,#2802,#1621,.T.);
#3546=EDGE_CURVE('',#2802,#2822,#1622,.T.);
#3547=EDGE_CURVE('',#2822,#2817,#1623,.T.);
#3548=EDGE_CURVE('',#2822,#2801,#1624,.T.);
#3549=EDGE_CURVE('',#2801,#2823,#1625,.T.);
#3550=EDGE_CURVE('',#2823,#2818,#1626,.T.);
#3551=EDGE_CURVE('',#2823,#2806,#1627,.T.);
#3552=EDGE_CURVE('',#2806,#2824,#1628,.T.);
#3553=EDGE_CURVE('',#2824,#2819,#1629,.T.);
#3554=EDGE_CURVE('',#2824,#2805,#1630,.T.);
#3555=EDGE_CURVE('',#2805,#2825,#1631,.T.);
#3556=EDGE_CURVE('',#2825,#2814,#1632,.T.);
#3557=EDGE_CURVE('',#2825,#2804,#1633,.T.);
#3558=EDGE_CURVE('',#2804,#2820,#1634,.T.);
#4921=ORIENTED_EDGE('',*,*,#3517,.T.);
#4922=ORIENTED_EDGE('',*,*,#3518,.T.);
#4923=ORIENTED_EDGE('',*,*,#3519,.T.);
#4924=ORIENTED_EDGE('',*,*,#3520,.T.);
#4925=ORIENTED_EDGE('',*,*,#3521,.T.);
#4926=ORIENTED_EDGE('',*,*,#3522,.T.);
#4927=ORIENTED_EDGE('',*,*,#3523,.T.);
#4928=ORIENTED_EDGE('',*,*,#3517,.F.);
#4929=ORIENTED_EDGE('',*,*,#3524,.F.);
#4930=ORIENTED_EDGE('',*,*,#3525,.T.);
#4931=ORIENTED_EDGE('',*,*,#3526,.F.);
#4932=ORIENTED_EDGE('',*,*,#3525,.F.);
#4933=ORIENTED_EDGE('',*,*,#3527,.F.);
#4934=ORIENTED_EDGE('',*,*,#3528,.T.);
#4935=ORIENTED_EDGE('',*,*,#3529,.T.);
#4936=ORIENTED_EDGE('',*,*,#3528,.F.);
#4937=ORIENTED_EDGE('',*,*,#3526,.T.);
#4938=ORIENTED_EDGE('',*,*,#3530,.T.);
#4939=ORIENTED_EDGE('',*,*,#3527,.T.);
#4940=ORIENTED_EDGE('',*,*,#3530,.F.);
#4941=ORIENTED_EDGE('',*,*,#3531,.F.);
#4942=ORIENTED_EDGE('',*,*,#3532,.T.);
#4943=ORIENTED_EDGE('',*,*,#3533,.T.);
#4944=ORIENTED_EDGE('',*,*,#3532,.F.);
#4945=ORIENTED_EDGE('',*,*,#3531,.T.);
#4946=ORIENTED_EDGE('',*,*,#3534,.F.);
#4947=ORIENTED_EDGE('',*,*,#3534,.T.);
#4948=ORIENTED_EDGE('',*,*,#3535,.T.);
#4949=ORIENTED_EDGE('',*,*,#3536,.T.);
#4950=ORIENTED_EDGE('',*,*,#3537,.T.);
#4951=ORIENTED_EDGE('',*,*,#3538,.T.);
#4952=ORIENTED_EDGE('',*,*,#3539,.T.);
#4953=ORIENTED_EDGE('',*,*,#3540,.T.);
#4954=ORIENTED_EDGE('',*,*,#3533,.F.);
#4955=ORIENTED_EDGE('',*,*,#3524,.T.);
#4956=ORIENTED_EDGE('',*,*,#3529,.F.);
#4957=ORIENTED_EDGE('',*,*,#3541,.T.);
#4958=ORIENTED_EDGE('',*,*,#3542,.T.);
#4959=ORIENTED_EDGE('',*,*,#3543,.T.);
#4960=ORIENTED_EDGE('',*,*,#3536,.F.);
#4961=ORIENTED_EDGE('',*,*,#3544,.F.);
#4962=ORIENTED_EDGE('',*,*,#3545,.T.);
#4963=ORIENTED_EDGE('',*,*,#3546,.T.);
#4964=ORIENTED_EDGE('',*,*,#3547,.T.);
#4965=ORIENTED_EDGE('',*,*,#3537,.F.);
#4966=ORIENTED_EDGE('',*,*,#3543,.F.);
#4967=ORIENTED_EDGE('',*,*,#3548,.T.);
#4968=ORIENTED_EDGE('',*,*,#3549,.T.);
#4969=ORIENTED_EDGE('',*,*,#3550,.T.);
#4970=ORIENTED_EDGE('',*,*,#3538,.F.);
#4971=ORIENTED_EDGE('',*,*,#3547,.F.);
#4972=ORIENTED_EDGE('',*,*,#3551,.T.);
#4973=ORIENTED_EDGE('',*,*,#3552,.T.);
#4974=ORIENTED_EDGE('',*,*,#3553,.T.);
#4975=ORIENTED_EDGE('',*,*,#3539,.F.);
#4976=ORIENTED_EDGE('',*,*,#3550,.F.);
#4977=ORIENTED_EDGE('',*,*,#3554,.T.);
#4978=ORIENTED_EDGE('',*,*,#3555,.T.);
#4979=ORIENTED_EDGE('',*,*,#3556,.T.);
#4980=ORIENTED_EDGE('',*,*,#3540,.F.);
#4981=ORIENTED_EDGE('',*,*,#3553,.F.);
#4982=ORIENTED_EDGE('',*,*,#3557,.T.);
#4983=ORIENTED_EDGE('',*,*,#3558,.T.);
#4984=ORIENTED_EDGE('',*,*,#3544,.T.);
#4985=ORIENTED_EDGE('',*,*,#3535,.F.);
#4986=ORIENTED_EDGE('',*,*,#3556,.F.);
#4987=ORIENTED_EDGE('',*,*,#3523,.F.);
#4988=ORIENTED_EDGE('',*,*,#3551,.F.);
#4989=ORIENTED_EDGE('',*,*,#3549,.F.);
#4990=ORIENTED_EDGE('',*,*,#3522,.F.);
#4991=ORIENTED_EDGE('',*,*,#3554,.F.);
#4992=ORIENTED_EDGE('',*,*,#3552,.F.);
#4993=ORIENTED_EDGE('',*,*,#3521,.F.);
#4994=ORIENTED_EDGE('',*,*,#3557,.F.);
#4995=ORIENTED_EDGE('',*,*,#3555,.F.);
#4996=ORIENTED_EDGE('',*,*,#3520,.F.);
#4997=ORIENTED_EDGE('',*,*,#3541,.F.);
#4998=ORIENTED_EDGE('',*,*,#3558,.F.);
#4999=ORIENTED_EDGE('',*,*,#3519,.F.);
#5000=ORIENTED_EDGE('',*,*,#3545,.F.);
#5001=ORIENTED_EDGE('',*,*,#3542,.F.);
#5002=ORIENTED_EDGE('',*,*,#3518,.F.);
#5003=ORIENTED_EDGE('',*,*,#3548,.F.);
#5004=ORIENTED_EDGE('',*,*,#3546,.F.);
#5261=CYLINDRICAL_SURFACE('',#6094,2.);
#5262=CYLINDRICAL_SURFACE('',#6095,3.8);
#5515=ADVANCED_FACE('',(#798),#161,.F.);
#5516=ADVANCED_FACE('',(#799),#156,.F.);
#5517=ADVANCED_FACE('',(#800),#162,.T.);
#5518=ADVANCED_FACE('',(#801),#5261,.T.);
#5519=ADVANCED_FACE('',(#802),#5262,.T.);
#5520=ADVANCED_FACE('',(#803,#380),#152,.T.);
#5521=ADVANCED_FACE('',(#804,#381),#505,.T.);
#5522=ADVANCED_FACE('',(#805,#382),#506,.F.);
#5523=ADVANCED_FACE('',(#806),#507,.F.);
#5524=ADVANCED_FACE('',(#807),#508,.T.);
#5525=ADVANCED_FACE('',(#808),#509,.T.);
#5526=ADVANCED_FACE('',(#809),#510,.T.);
#5527=ADVANCED_FACE('',(#810),#511,.T.);
#5528=ADVANCED_FACE('',(#811),#512,.T.);
#5529=ADVANCED_FACE('',(#812),#513,.T.);
#5530=ADVANCED_FACE('',(#813),#514,.F.);
#5531=ADVANCED_FACE('',(#814),#515,.F.);
#5532=ADVANCED_FACE('',(#815),#516,.F.);
#5533=ADVANCED_FACE('',(#816),#517,.F.);
#5534=ADVANCED_FACE('',(#817),#518,.F.);
#5535=ADVANCED_FACE('',(#818),#519,.F.);
#5587=CLOSED_SHELL('',(#5515,#5516,#5517,#5518,#5519,#5520,#5521,#5522,
#5523,#5524,#5525,#5526,#5527,#5528,#5529,#5530,#5531,#5532,#5533,#5534,
#5535));
#6079=AXIS2_PLACEMENT_3D('',#12642,#7395,#7396);
#6080=AXIS2_PLACEMENT_3D('',#12643,#7397,#7398);
#6081=AXIS2_PLACEMENT_3D('',#12648,#7400,#7401);
#6082=AXIS2_PLACEMENT_3D('',#12650,#7402,#7403);
#6083=AXIS2_PLACEMENT_3D('',#12652,#7404,#7405);
#6084=AXIS2_PLACEMENT_3D('',#12654,#7406,#7407);
#6085=AXIS2_PLACEMENT_3D('',#12656,#7408,#7409);
#6086=AXIS2_PLACEMENT_3D('',#12657,#7410,#7411);
#6087=AXIS2_PLACEMENT_3D('',#12658,#7412,#7413);
#6088=AXIS2_PLACEMENT_3D('',#12660,#7414,#7415);
#6089=AXIS2_PLACEMENT_3D('',#12662,#7416,#7417);
#6090=AXIS2_PLACEMENT_3D('',#12663,#7418,#7419);
#6091=AXIS2_PLACEMENT_3D('',#12664,#7420,#7421);
#6092=AXIS2_PLACEMENT_3D('',#12666,#7422,#7423);
#6093=AXIS2_PLACEMENT_3D('',#12669,#7425,#7426);
#6094=AXIS2_PLACEMENT_3D('',#12670,#7427,#7428);
#6095=AXIS2_PLACEMENT_3D('',#12672,#7430,#7431);
#6096=AXIS2_PLACEMENT_3D('',#12674,#7432,#7433);
#6097=AXIS2_PLACEMENT_3D('',#12677,#7435,#7436);
#6098=AXIS2_PLACEMENT_3D('',#12678,#7437,#7438);
#6099=AXIS2_PLACEMENT_3D('',#12680,#7439,#7440);
#6100=AXIS2_PLACEMENT_3D('',#12681,#7441,#7442);
#6101=AXIS2_PLACEMENT_3D('',#12694,#7449,#7450);
#6102=AXIS2_PLACEMENT_3D('',#12695,#7451,#7452);
#6103=AXIS2_PLACEMENT_3D('',#12696,#7453,#7454);
#6104=AXIS2_PLACEMENT_3D('',#12703,#7459,#7460);
#6105=AXIS2_PLACEMENT_3D('',#12708,#7464,#7465);
#6106=AXIS2_PLACEMENT_3D('',#12713,#7469,#7470);
#6107=AXIS2_PLACEMENT_3D('',#12718,#7474,#7475);
#6108=AXIS2_PLACEMENT_3D('',#12723,#7479,#7480);
#6109=AXIS2_PLACEMENT_3D('',#12726,#7483,#7484);
#6110=AXIS2_PLACEMENT_3D('',#12727,#7485,#7486);
#6111=AXIS2_PLACEMENT_3D('',#12728,#7487,#7488);
#6112=AXIS2_PLACEMENT_3D('',#12729,#7489,#7490);
#6113=AXIS2_PLACEMENT_3D('',#12730,#7491,#7492);
#6114=AXIS2_PLACEMENT_3D('',#12731,#7493,#7494);
#7395=DIRECTION('axis',(0.,0.,1.));
#7396=DIRECTION('refdir',(1.,0.,0.));
#7397=DIRECTION('center_axis',(-1.,-2.97906491917051E-43,0.));
#7398=DIRECTION('ref_axis',(0.,0.,1.));
#7399=DIRECTION('',(-0.500000000000004,-1.0605752387249E-16,-0.866025403784436));
#7400=DIRECTION('center_axis',(-1.,-2.97906491917051E-43,0.));
#7401=DIRECTION('ref_axis',(0.,0.,1.));
#7402=DIRECTION('center_axis',(-1.,-2.97906491917051E-43,0.));
#7403=DIRECTION('ref_axis',(0.,0.,1.));
#7404=DIRECTION('center_axis',(-1.,-2.97906491917051E-43,0.));
#7405=DIRECTION('ref_axis',(0.,0.,1.));
#7406=DIRECTION('center_axis',(-1.,-2.97906491917051E-43,0.));
#7407=DIRECTION('ref_axis',(0.,0.,1.));
#7408=DIRECTION('center_axis',(-1.,-2.97906491917051E-43,0.));
#7409=DIRECTION('ref_axis',(0.,0.,1.));
#7410=DIRECTION('center_axis',(-1.,-2.97906491917051E-43,0.));
#7411=DIRECTION('ref_axis',(0.,0.,1.));
#7412=DIRECTION('center_axis',(-1.,-2.97906491917051E-43,0.));
#7413=DIRECTION('ref_axis',(0.,0.,1.));
#7414=DIRECTION('center_axis',(-1.,-2.97906491917051E-43,0.));
#7415=DIRECTION('ref_axis',(0.,0.,1.));
#7416=DIRECTION('center_axis',(-2.97906491917051E-43,1.,-1.22464679914735E-16));
#7417=DIRECTION('ref_axis',(0.,-1.22464679914735E-16,-1.));
#7418=DIRECTION('center_axis',(1.,2.97906491917051E-43,0.));
#7419=DIRECTION('ref_axis',(0.,0.,1.));
#7420=DIRECTION('center_axis',(-1.,-2.97906491917051E-43,0.));
#7421=DIRECTION('ref_axis',(0.,0.,1.));
#7422=DIRECTION('center_axis',(-1.,-2.97906491917051E-43,0.));
#7423=DIRECTION('ref_axis',(0.,0.,1.));
#7424=DIRECTION('',(0.707106781186549,8.65956056235492E-17,0.707106781186547));
#7425=DIRECTION('center_axis',(-1.,-2.97906491917051E-43,0.));
#7426=DIRECTION('ref_axis',(0.,0.,1.));
#7427=DIRECTION('center_axis',(-1.,-2.97906491917051E-43,0.));
#7428=DIRECTION('ref_axis',(0.,0.,1.));
#7429=DIRECTION('',(1.,2.97906491917051E-43,0.));
#7430=DIRECTION('center_axis',(-1.,-2.97906491917051E-43,0.));
#7431=DIRECTION('ref_axis',(0.,0.,1.));
#7432=DIRECTION('center_axis',(-1.,-2.97906491917051E-43,0.));
#7433=DIRECTION('ref_axis',(0.,0.,1.));
#7434=DIRECTION('',(1.,2.97906491917051E-43,0.));
#7435=DIRECTION('center_axis',(-1.,-2.97906491917051E-43,0.));
#7436=DIRECTION('ref_axis',(0.,0.,1.));
#7437=DIRECTION('center_axis',(0.,6.12323399573677E-17,-1.));
#7438=DIRECTION('ref_axis',(0.,1.,0.));
#7439=DIRECTION('center_axis',(-1.,-2.97906491917051E-43,0.));
#7440=DIRECTION('ref_axis',(0.,0.,1.));
#7441=DIRECTION('center_axis',(-1.,-2.97906491917051E-43,0.));
#7442=DIRECTION('ref_axis',(0.,0.,1.));
#7443=DIRECTION('',(8.19972511286966E-38,-1.,1.50231459873716E-16));
#7444=DIRECTION('',(9.4039548065783E-38,-0.5,-0.866025403784438));
#7445=DIRECTION('',(0.,0.5,-0.866025403784438));
#7446=DIRECTION('',(2.97906491917051E-43,1.,0.));
#7447=DIRECTION('',(-9.4039548065783E-38,0.5,0.866025403784438));
#7448=DIRECTION('',(0.,-0.5,0.866025403784438));
#7449=DIRECTION('center_axis',(-1.,-2.97906491917051E-43,0.));
#7450=DIRECTION('ref_axis',(0.,0.,1.));
#7451=DIRECTION('center_axis',(-1.,-2.97906491917051E-43,0.));
#7452=DIRECTION('ref_axis',(0.,0.,1.));
#7453=DIRECTION('center_axis',(4.70197740328915E-38,0.866025403784438,-0.5));
#7454=DIRECTION('ref_axis',(-9.4039548065783E-38,0.5,0.866025403784438));
#7455=DIRECTION('',(9.4039548065783E-38,-0.5,-0.866025403784438));
#7456=DIRECTION('',(9.4039548065783E-38,-0.5,-0.866025403784438));
#7457=DIRECTION('',(-1.,-2.97906491917051E-43,0.));
#7458=DIRECTION('',(-1.,-2.97906491917051E-43,0.));
#7459=DIRECTION('center_axis',(9.4039548065783E-38,0.866025403784438,0.5));
#7460=DIRECTION('ref_axis',(-4.84544694858195E-54,-0.5,0.866025403784438));
#7461=DIRECTION('',(0.,0.5,-0.866025403784438));
#7462=DIRECTION('',(0.,0.5,-0.866025403784438));
#7463=DIRECTION('',(-1.,-2.97906491917051E-43,0.));
#7464=DIRECTION('center_axis',(0.,0.,1.));
#7465=DIRECTION('ref_axis',(1.,2.97906491917051E-43,0.));
#7466=DIRECTION('',(2.97906491917051E-43,1.,0.));
#7467=DIRECTION('',(2.97906491917051E-43,1.,0.));
#7468=DIRECTION('',(-1.,-2.97906491917051E-43,0.));
#7469=DIRECTION('center_axis',(-4.70197740328915E-38,-0.866025403784439,
0.5));
#7470=DIRECTION('ref_axis',(9.4039548065783E-38,-0.5,-0.866025403784439));
#7471=DIRECTION('',(-9.4039548065783E-38,0.5,0.866025403784438));
#7472=DIRECTION('',(-9.4039548065783E-38,0.5,0.866025403784438));
#7473=DIRECTION('',(-1.,-2.97906491917051E-43,0.));
#7474=DIRECTION('center_axis',(-4.70197740328915E-38,-0.866025403784439,
-0.5));
#7475=DIRECTION('ref_axis',(3.12210349931794E-54,0.5,-0.866025403784439));
#7476=DIRECTION('',(0.,-0.5,0.866025403784438));
#7477=DIRECTION('',(0.,-0.5,0.866025403784438));
#7478=DIRECTION('',(-1.,-2.97906491917051E-43,0.));
#7479=DIRECTION('center_axis',(0.,-1.50231459873716E-16,-1.));
#7480=DIRECTION('ref_axis',(-8.19972511286966E-38,1.,-1.50231459873716E-16));
#7481=DIRECTION('',(8.19972511286966E-38,-1.,1.50231459873716E-16));
#7482=DIRECTION('',(8.19972511286966E-38,-1.,1.50231459873716E-16));
#7483=DIRECTION('center_axis',(1.,2.97906491917051E-43,0.));
#7484=DIRECTION('ref_axis',(0.,0.,-1.));
#7485=DIRECTION('center_axis',(1.,2.97906491917051E-43,0.));
#7486=DIRECTION('ref_axis',(0.,0.,-1.));
#7487=DIRECTION('center_axis',(1.,2.97906491917051E-43,0.));
#7488=DIRECTION('ref_axis',(0.,0.,-1.));
#7489=DIRECTION('center_axis',(1.,2.97906491917051E-43,0.));
#7490=DIRECTION('ref_axis',(0.,0.,-1.));
#7491=DIRECTION('center_axis',(1.,2.97906491917051E-43,0.));
#7492=DIRECTION('ref_axis',(0.,0.,-1.));
#7493=DIRECTION('center_axis',(1.,2.97906491917051E-43,0.));
#7494=DIRECTION('ref_axis',(0.,0.,-1.));
#12642=CARTESIAN_POINT('',(0.,0.,0.));
#12643=CARTESIAN_POINT('Origin',(-997.978312163513,-2.97906491917051E-40,
0.));
#12644=CARTESIAN_POINT('',(2.02168783648704,0.,0.));
#12645=CARTESIAN_POINT('',(1.30000000000002,0.,-1.25));
#12646=CARTESIAN_POINT('',(-997.978312163513,-2.12115047744979E-13,-1732.05080756886));
#12647=CARTESIAN_POINT('',(1.30000000000002,-1.08253175473055,-0.624999999999987));
#12648=CARTESIAN_POINT('Origin',(1.30000000000002,0.,0.));
#12649=CARTESIAN_POINT('',(1.30000000000002,-1.08253175473055,0.624999999999987));
#12650=CARTESIAN_POINT('Origin',(1.30000000000002,0.,0.));
#12651=CARTESIAN_POINT('',(1.30000000000002,0.,1.25));
#12652=CARTESIAN_POINT('Origin',(1.30000000000002,0.,0.));
#12653=CARTESIAN_POINT('',(1.30000000000002,1.08253175473055,0.625000000000014));
#12654=CARTESIAN_POINT('Origin',(1.30000000000002,0.,0.));
#12655=CARTESIAN_POINT('',(1.30000000000002,1.08253175473055,-0.624999999999987));
#12656=CARTESIAN_POINT('Origin',(1.30000000000002,0.,0.));
#12657=CARTESIAN_POINT('Origin',(1.30000000000002,0.,0.));
#12658=CARTESIAN_POINT('Origin',(2.40000000000001,0.,0.));
#12659=CARTESIAN_POINT('',(2.19999999999998,-2.69422295812418E-16,-2.2));
#12660=CARTESIAN_POINT('Origin',(2.19999999999998,0.,0.));
#12661=CARTESIAN_POINT('',(2.40000000000001,-2.44929359829471E-16,-2.));
#12662=CARTESIAN_POINT('Origin',(2.40000000000001,-2.69422295812418E-16,
-2.2));
#12663=CARTESIAN_POINT('Origin',(2.40000000000001,0.,0.));
#12664=CARTESIAN_POINT('Origin',(10.2,0.,0.));
#12665=CARTESIAN_POINT('',(9.80999999999999,-2.44929359829471E-16,-2.));
#12666=CARTESIAN_POINT('Origin',(9.80999999999998,0.,0.));
#12667=CARTESIAN_POINT('',(10.2,-1.97168134662724E-16,-1.61));
#12668=CARTESIAN_POINT('',(10.2,-1.97168134662724E-16,-1.61));
#12669=CARTESIAN_POINT('Origin',(10.2,0.,0.));
#12670=CARTESIAN_POINT('Origin',(0.,0.,0.));
#12671=CARTESIAN_POINT('',(7.29660463542866E-59,-2.44929359829471E-16,-2.));
#12672=CARTESIAN_POINT('Origin',(0.,0.,0.));
#12673=CARTESIAN_POINT('',(1.81999999999999,-4.65365783675994E-16,-3.8));
#12674=CARTESIAN_POINT('Origin',(1.81999999999999,0.,0.));
#12675=CARTESIAN_POINT('',(2.19999999999998,-4.65365783675994E-16,-3.8));
#12676=CARTESIAN_POINT('',(1.38635488073145E-58,-4.65365783675994E-16,-3.8));
#12677=CARTESIAN_POINT('Origin',(2.19999999999998,0.,0.));
#12678=CARTESIAN_POINT('Origin',(3.88527472527472,0.,0.));
#12679=CARTESIAN_POINT('',(-5.66022334642396E-43,1.9,0.));
#12680=CARTESIAN_POINT('Origin',(0.,0.,0.));
#12681=CARTESIAN_POINT('Origin',(0.,0.,0.));
#12682=CARTESIAN_POINT('',(0.,0.721687836487031,1.25));
#12683=CARTESIAN_POINT('',(0.,-0.721687836487031,1.25));
#12684=CARTESIAN_POINT('',(0.,-0.721687836487031,1.25));
#12685=CARTESIAN_POINT('',(0.,-1.44337567297407,0.));
#12686=CARTESIAN_POINT('',(0.,-1.44337567297407,0.));
#12687=CARTESIAN_POINT('',(0.,-0.721687836487031,-1.25));
#12688=CARTESIAN_POINT('',(0.,-0.721687836487031,-1.25));
#12689=CARTESIAN_POINT('',(0.,0.721687836487031,-1.25));
#12690=CARTESIAN_POINT('',(0.,0.721687836487031,-1.25));
#12691=CARTESIAN_POINT('',(0.,1.44337567297407,0.));
#12692=CARTESIAN_POINT('',(0.,1.44337567297407,0.));
#12693=CARTESIAN_POINT('',(0.,0.721687836487031,1.25));
#12694=CARTESIAN_POINT('Origin',(2.19999999999998,2.,0.));
#12695=CARTESIAN_POINT('Origin',(10.2,0.,0.));
#12696=CARTESIAN_POINT('Origin',(1.30000000000002,-1.44337567297407,0.));
#12697=CARTESIAN_POINT('',(1.30000000000002,-0.721687836487031,1.25));
#12698=CARTESIAN_POINT('',(1.30000000000002,-1.44337567297407,0.));
#12699=CARTESIAN_POINT('',(1.30000000000002,-1.44337567297407,0.));
#12700=CARTESIAN_POINT('',(1.30000000000002,-1.44337567297407,0.));
#12701=CARTESIAN_POINT('',(1.30000000000002,-1.44337567297407,0.));
#12702=CARTESIAN_POINT('',(1.30000000000002,-0.721687836487031,1.25));
#12703=CARTESIAN_POINT('Origin',(1.30000000000002,-0.721687836487031,-1.25));
#12704=CARTESIAN_POINT('',(1.30000000000002,-0.721687836487031,-1.25));
#12705=CARTESIAN_POINT('',(1.30000000000002,-0.721687836487031,-1.25));
#12706=CARTESIAN_POINT('',(1.30000000000002,-0.721687836487031,-1.25));
#12707=CARTESIAN_POINT('',(1.30000000000002,-0.721687836487031,-1.25));
#12708=CARTESIAN_POINT('Origin',(1.30000000000002,0.721687836487031,-1.25));
#12709=CARTESIAN_POINT('',(1.30000000000002,0.721687836487031,-1.25));
#12710=CARTESIAN_POINT('',(1.30000000000002,0.721687836487031,-1.25));
#12711=CARTESIAN_POINT('',(1.30000000000002,0.721687836487031,-1.25));
#12712=CARTESIAN_POINT('',(1.30000000000002,0.721687836487031,-1.25));
#12713=CARTESIAN_POINT('Origin',(1.30000000000002,1.44337567297407,0.));
#12714=CARTESIAN_POINT('',(1.30000000000002,1.44337567297407,0.));
#12715=CARTESIAN_POINT('',(1.30000000000002,1.44337567297407,0.));
#12716=CARTESIAN_POINT('',(1.30000000000002,1.44337567297407,0.));
#12717=CARTESIAN_POINT('',(1.30000000000002,1.44337567297407,0.));
#12718=CARTESIAN_POINT('Origin',(1.30000000000002,0.721687836487031,1.25));
#12719=CARTESIAN_POINT('',(1.30000000000002,0.721687836487031,1.25));
#12720=CARTESIAN_POINT('',(1.30000000000002,0.721687836487031,1.25));
#12721=CARTESIAN_POINT('',(1.30000000000002,0.721687836487031,1.25));
#12722=CARTESIAN_POINT('',(1.30000000000002,0.721687836487031,1.25));
#12723=CARTESIAN_POINT('Origin',(1.30000000000002,-0.721687836487031,1.25));
#12724=CARTESIAN_POINT('',(1.30000000000002,-0.721687836487031,1.25));
#12725=CARTESIAN_POINT('',(1.30000000000002,-0.721687836487031,1.25));
#12726=CARTESIAN_POINT('Origin',(1.30000000000002,-1.44337567297407,0.));
#12727=CARTESIAN_POINT('Origin',(1.30000000000002,-1.44337567297407,0.));
#12728=CARTESIAN_POINT('Origin',(1.30000000000002,-1.44337567297407,0.));
#12729=CARTESIAN_POINT('Origin',(1.30000000000002,-1.44337567297407,0.));
#12730=CARTESIAN_POINT('Origin',(1.30000000000002,-1.44337567297407,0.));
#12731=CARTESIAN_POINT('Origin',(1.30000000000002,-1.44337567297407,0.));
#12953=UNCERTAINTY_MEASURE_WITH_UNIT(LENGTH_MEASURE(0.01),#12967,
'DISTANCE_ACCURACY_VALUE',
'Maximum model space distance between geometric entities at asserted c
onnectivities');
#12956=UNCERTAINTY_MEASURE_WITH_UNIT(LENGTH_MEASURE(0.01),#12967,
'DISTANCE_ACCURACY_VALUE',
'Maximum model space distance between geometric entities at asserted c
onnectivities');
#12963=(
GEOMETRIC_REPRESENTATION_CONTEXT(3)
GLOBAL_UNCERTAINTY_ASSIGNED_CONTEXT((#12953))
GLOBAL_UNIT_ASSIGNED_CONTEXT((#12967,#12969,#12970))
REPRESENTATION_CONTEXT('','3D')
);
#12966=(
GEOMETRIC_REPRESENTATION_CONTEXT(3)
GLOBAL_UNCERTAINTY_ASSIGNED_CONTEXT((#12956))
GLOBAL_UNIT_ASSIGNED_CONTEXT((#12967,#12969,#12970))
REPRESENTATION_CONTEXT('','3D')
);
#12967=(
LENGTH_UNIT()
NAMED_UNIT(*)
SI_UNIT(.MILLI.,.METRE.)
);
#12969=(
NAMED_UNIT(*)
PLANE_ANGLE_UNIT()
SI_UNIT($,.RADIAN.)
);
#12970=(
NAMED_UNIT(*)
SI_UNIT($,.STERADIAN.)
SOLID_ANGLE_UNIT()
);
#12977=SHAPE_DEFINITION_REPRESENTATION(#12986,#13030);
#12986=PRODUCT_DEFINITION_SHAPE('',$,#13040);
#13030=SHAPE_REPRESENTATION('',(#6079),#12963);
#13033=PRODUCT_DEFINITION_CONTEXT('part definition',#13062,'design');
#13040=PRODUCT_DEFINITION('Button Head Cap Screw M4x0.7x8',
'Button Head Cap Screw M4x0.7x8',#13049,#13033);
#13049=PRODUCT_DEFINITION_FORMATION('',$,#13070);
#13062=APPLICATION_CONTEXT(
'Core Data for Automotive Mechanical Design Process');
#13063=PRODUCT_CONTEXT('part definition',#13062,'mechanical');
#13070=PRODUCT('Button Head Cap Screw M4x0.7x8',
'Button Head Cap Screw M4x0.7x8',$,(#13063));
#13075=PRESENTATION_STYLE_ASSIGNMENT((#13080));
#13080=SURFACE_STYLE_USAGE(.BOTH.,#13085);
#13085=SURFACE_SIDE_STYLE('',(#13090));
#13090=SURFACE_STYLE_FILL_AREA(#13095);
#13095=FILL_AREA_STYLE('Opaque(31,36,43)',(#13100));
#13100=FILL_AREA_STYLE_COLOUR('Opaque(31,36,43)',#13105);
#13105=COLOUR_RGB('Opaque(31,36,43)',0.12156862745098,0.141176470588235,
0.168627450980392);
ENDSEC;
END-ISO-10303-21;
